ISO-10303-21;
HEADER;
/* Generated by software containing ST-Developer
 * from STEP Tools, Inc. (www.steptools.com) 
 */

FILE_DESCRIPTION(
/* description */ ('Line shaft on three pillow blocks'),
/* implementation_level */ '2;1');

FILE_NAME(
/* name */ 'End collar (1).step',
/* time_stamp */ '2026-10-27T10:49:19-07:00',
/* author */ (''),
/* organization */ (''),
/* preprocessor_version */ 'ST-DEVELOPER v20.2',
/* originating_system */ 'Autodesk Translation Framework v15.17.0.0',
/* authorisation */ '');

FILE_SCHEMA (('AUTOMOTIVE_DESIGN { 1 0 10303 214 3 1 1 }'));
ENDSEC;

DATA;
#10=MECHANICAL_DESIGN_GEOMETRIC_PRESENTATION_REPRESENTATION('',(#360),#8377);
#259=B_SPLINE_CURVE_WITH_KNOTS('',3,(#8005,#8006,#8007,#8008,#8009,#8010,
#8011,#8012,#8013,#8014,#8015,#8016,#8017,#8018),.UNSPECIFIED.,.F.,.F.,
(4,2,2,2,2,2,4),(0.756005737987015,0.793568827564645,0.8729225200542,0.952276212543755,
1.03162990503331,1.11098359752287,1.1485466871005),.UNSPECIFIED.);
#260=B_SPLINE_CURVE_WITH_KNOTS('',3,(#8024,#8025,#8026,#8027,#8028,#8029,
#8030,#8031,#8032,#8033,#8034,#8035,#8036,#8037,#8038,#8039,#8040,#8041),
 .UNSPECIFIED.,.F.,.F.,(4,2,2,2,2,2,2,2,4),(0.,0.0792165807733624,0.158433161546725,
0.237648697074569,0.316864232602414,0.396079768130259,0.475295303658103,
0.554511884431466,0.633728465204828),.UNSPECIFIED.);
#261=B_SPLINE_CURVE_WITH_KNOTS('',3,(#8042,#8043,#8044,#8045,#8046,#8047,
#8048,#8049,#8050,#8051,#8052,#8053,#8054,#8055,#8056,#8057,#8058,#8059),
 .UNSPECIFIED.,.F.,.F.,(4,2,2,2,2,2,2,2,4),(0.633728465204828,0.712945045978191,
0.792161626751553,0.871377162279398,0.950592697807242,1.02980823333509,
1.10902376886293,1.18824034963629,1.26745693040966),.UNSPECIFIED.);
#262=B_SPLINE_CURVE_WITH_KNOTS('',3,(#8062,#8063,#8064,#8065,#8066,#8067,
#8068,#8069,#8070,#8071,#8072,#8073,#8074,#8075),.UNSPECIFIED.,.F.,.F.,
(4,2,2,2,2,2,4),(0.121154929624512,0.158718019202141,0.238071711691696,
0.317425404181252,0.396779096670807,0.476132789160362,0.513695878737992),
 .UNSPECIFIED.);
#305=SHAPE_REPRESENTATION_RELATIONSHIP('SRR','None',#8522,#332);
#332=ADVANCED_BREP_SHAPE_REPRESENTATION('',(#386),#8371);
#360=STYLED_ITEM('',(#8704),#386);
#386=MANIFOLD_SOLID_BREP('Body1',#4348);
#478=FACE_BOUND('',#1195,.T.);
#479=FACE_BOUND('',#1197,.T.);
#480=FACE_BOUND('',#1199,.T.);
#481=FACE_BOUND('',#1201,.T.);
#616=PLANE('',#5045);
#617=PLANE('',#5050);
#618=PLANE('',#5057);
#619=PLANE('',#5058);
#852=FACE_OUTER_BOUND('',#1191,.T.);
#853=FACE_OUTER_BOUND('',#1192,.T.);
#854=FACE_OUTER_BOUND('',#1193,.T.);
#855=FACE_OUTER_BOUND('',#1194,.T.);
#856=FACE_OUTER_BOUND('',#1196,.T.);
#857=FACE_OUTER_BOUND('',#1198,.T.);
#858=FACE_OUTER_BOUND('',#1200,.T.);
#1191=EDGE_LOOP('',(#3783,#3784));
#1192=EDGE_LOOP('',(#3785,#3786,#3787,#3788,#3789,#3790,#3791,#3792,#3793));
#1193=EDGE_LOOP('',(#3794,#3795,#3796));
#1194=EDGE_LOOP('',(#3797,#3798,#3799,#3800));
#1195=EDGE_LOOP('',(#3801,#3802,#3803,#3804));
#1196=EDGE_LOOP('',(#3805,#3806,#3807,#3808));
#1197=EDGE_LOOP('',(#3809,#3810));
#1198=EDGE_LOOP('',(#3811));
#1199=EDGE_LOOP('',(#3812));
#1200=EDGE_LOOP('',(#3813));
#1201=EDGE_LOOP('',(#3814));
#1504=LINE('',#8001,#1831);
#1505=LINE('',#8022,#1832);
#1506=LINE('',#8077,#1833);
#1507=LINE('',#8082,#1834);
#1508=LINE('',#8088,#1835);
#1831=VECTOR('',#6183,1.);
#1832=VECTOR('',#6190,0.21);
#1833=VECTOR('',#6195,1.);
#1834=VECTOR('',#6200,1.005);
#1835=VECTOR('',#6207,1.5);
#2041=CIRCLE('',#5046,0.21);
#2042=CIRCLE('',#5048,0.21);
#2043=CIRCLE('',#5049,0.21);
#2044=CIRCLE('',#5052,1.005);
#2045=CIRCLE('',#5053,1.005);
#2046=CIRCLE('',#5055,1.5);
#2047=CIRCLE('',#5056,1.5);
#2352=VERTEX_POINT('',#7999);
#2353=VERTEX_POINT('',#8000);
#2354=VERTEX_POINT('',#8004);
#2355=VERTEX_POINT('',#8019);
#2356=VERTEX_POINT('',#8021);
#2357=VERTEX_POINT('',#8023);
#2358=VERTEX_POINT('',#8060);
#2359=VERTEX_POINT('',#8079);
#2360=VERTEX_POINT('',#8081);
#2361=VERTEX_POINT('',#8085);
#2362=VERTEX_POINT('',#8087);
#2840=EDGE_CURVE('',#2352,#2353,#1504,.T.);
#2841=EDGE_CURVE('',#2352,#2353,#2041,.T.);
#2842=EDGE_CURVE('',#2354,#2352,#259,.T.);
#2843=EDGE_CURVE('',#2355,#2354,#2042,.T.);
#2844=EDGE_CURVE('',#2355,#2356,#1505,.T.);
#2845=EDGE_CURVE('',#2357,#2356,#260,.T.);
#2846=EDGE_CURVE('',#2356,#2357,#261,.T.);
#2847=EDGE_CURVE('',#2358,#2355,#2043,.T.);
#2848=EDGE_CURVE('',#2353,#2358,#262,.T.);
#2849=EDGE_CURVE('',#2358,#2354,#1506,.T.);
#2850=EDGE_CURVE('',#2359,#2359,#2044,.T.);
#2851=EDGE_CURVE('',#2359,#2360,#1507,.T.);
#2852=EDGE_CURVE('',#2360,#2360,#2045,.T.);
#2853=EDGE_CURVE('',#2361,#2361,#2046,.T.);
#2854=EDGE_CURVE('',#2361,#2362,#1508,.T.);
#2855=EDGE_CURVE('',#2362,#2362,#2047,.T.);
#3783=ORIENTED_EDGE('',*,*,#2840,.F.);
#3784=ORIENTED_EDGE('',*,*,#2841,.T.);
#3785=ORIENTED_EDGE('',*,*,#2842,.F.);
#3786=ORIENTED_EDGE('',*,*,#2843,.F.);
#3787=ORIENTED_EDGE('',*,*,#2844,.T.);
#3788=ORIENTED_EDGE('',*,*,#2845,.F.);
#3789=ORIENTED_EDGE('',*,*,#2846,.F.);
#3790=ORIENTED_EDGE('',*,*,#2844,.F.);
#3791=ORIENTED_EDGE('',*,*,#2847,.F.);
#3792=ORIENTED_EDGE('',*,*,#2848,.F.);
#3793=ORIENTED_EDGE('',*,*,#2841,.F.);
#3794=ORIENTED_EDGE('',*,*,#2849,.F.);
#3795=ORIENTED_EDGE('',*,*,#2847,.T.);
#3796=ORIENTED_EDGE('',*,*,#2843,.T.);
#3797=ORIENTED_EDGE('',*,*,#2850,.F.);
#3798=ORIENTED_EDGE('',*,*,#2851,.T.);
#3799=ORIENTED_EDGE('',*,*,#2852,.T.);
#3800=ORIENTED_EDGE('',*,*,#2851,.F.);
#3801=ORIENTED_EDGE('',*,*,#2848,.T.);
#3802=ORIENTED_EDGE('',*,*,#2849,.T.);
#3803=ORIENTED_EDGE('',*,*,#2842,.T.);
#3804=ORIENTED_EDGE('',*,*,#2840,.T.);
#3805=ORIENTED_EDGE('',*,*,#2853,.F.);
#3806=ORIENTED_EDGE('',*,*,#2854,.T.);
#3807=ORIENTED_EDGE('',*,*,#2855,.T.);
#3808=ORIENTED_EDGE('',*,*,#2854,.F.);
#3809=ORIENTED_EDGE('',*,*,#2845,.T.);
#3810=ORIENTED_EDGE('',*,*,#2846,.T.);
#3811=ORIENTED_EDGE('',*,*,#2853,.T.);
#3812=ORIENTED_EDGE('',*,*,#2850,.T.);
#3813=ORIENTED_EDGE('',*,*,#2855,.F.);
#3814=ORIENTED_EDGE('',*,*,#2852,.F.);
#4062=CYLINDRICAL_SURFACE('',#5047,0.21);
#4063=CYLINDRICAL_SURFACE('',#5051,1.005);
#4064=CYLINDRICAL_SURFACE('',#5054,1.5);
#4270=ADVANCED_FACE('',(#852),#616,.T.);
#4271=ADVANCED_FACE('',(#853),#4062,.F.);
#4272=ADVANCED_FACE('',(#854),#617,.T.);
#4273=ADVANCED_FACE('',(#855,#478),#4063,.F.);
#4274=ADVANCED_FACE('',(#856,#479),#4064,.T.);
#4275=ADVANCED_FACE('',(#857,#480),#618,.T.);
#4276=ADVANCED_FACE('',(#858,#481),#619,.F.);
#4348=CLOSED_SHELL('',(#4270,#4271,#4272,#4273,#4274,#4275,#4276));
#5044=AXIS2_PLACEMENT_3D('',#7997,#6179,#6180);
#5045=AXIS2_PLACEMENT_3D('',#7998,#6181,#6182);
#5046=AXIS2_PLACEMENT_3D('',#8002,#6184,#6185);
#5047=AXIS2_PLACEMENT_3D('',#8003,#6186,#6187);
#5048=AXIS2_PLACEMENT_3D('',#8020,#6188,#6189);
#5049=AXIS2_PLACEMENT_3D('',#8061,#6191,#6192);
#5050=AXIS2_PLACEMENT_3D('',#8076,#6193,#6194);
#5051=AXIS2_PLACEMENT_3D('',#8078,#6196,#6197);
#5052=AXIS2_PLACEMENT_3D('',#8080,#6198,#6199);
#5053=AXIS2_PLACEMENT_3D('',#8083,#6201,#6202);
#5054=AXIS2_PLACEMENT_3D('',#8084,#6203,#6204);
#5055=AXIS2_PLACEMENT_3D('',#8086,#6205,#6206);
#5056=AXIS2_PLACEMENT_3D('',#8089,#6208,#6209);
#5057=AXIS2_PLACEMENT_3D('',#8090,#6210,#6211);
#5058=AXIS2_PLACEMENT_3D('',#8091,#6212,#6213);
#6179=DIRECTION('axis',(0.,0.,1.));
#6180=DIRECTION('refdir',(1.,0.,0.));
#6181=DIRECTION('center_axis',(0.,0.,1.));
#6182=DIRECTION('ref_axis',(1.,0.,0.));
#6183=DIRECTION('',(0.,1.,0.));
#6184=DIRECTION('center_axis',(0.,0.,1.));
#6185=DIRECTION('ref_axis',(1.,0.,0.));
#6186=DIRECTION('center_axis',(0.,0.,1.));
#6187=DIRECTION('ref_axis',(1.,0.,0.));
#6188=DIRECTION('center_axis',(0.,0.,1.));
#6189=DIRECTION('ref_axis',(1.,0.,0.));
#6190=DIRECTION('',(0.,0.,1.));
#6191=DIRECTION('center_axis',(0.,0.,1.));
#6192=DIRECTION('ref_axis',(1.,0.,0.));
#6193=DIRECTION('center_axis',(0.,0.,1.));
#6194=DIRECTION('ref_axis',(1.,0.,0.));
#6195=DIRECTION('',(0.,-1.,0.));
#6196=DIRECTION('center_axis',(0.,1.,0.));
#6197=DIRECTION('ref_axis',(1.,0.,0.));
#6198=DIRECTION('center_axis',(0.,-1.,0.));
#6199=DIRECTION('ref_axis',(1.,0.,0.));
#6200=DIRECTION('',(0.,-1.,0.));
#6201=DIRECTION('center_axis',(0.,-1.,0.));
#6202=DIRECTION('ref_axis',(1.,0.,0.));
#6203=DIRECTION('center_axis',(0.,1.,0.));
#6204=DIRECTION('ref_axis',(1.,0.,0.));
#6205=DIRECTION('center_axis',(0.,1.,0.));
#6206=DIRECTION('ref_axis',(1.,0.,0.));
#6207=DIRECTION('',(0.,-1.,0.));
#6208=DIRECTION('center_axis',(0.,1.,0.));
#6209=DIRECTION('ref_axis',(1.,0.,0.));
#6210=DIRECTION('center_axis',(0.,1.,0.));
#6211=DIRECTION('ref_axis',(1.,0.,0.));
#6212=DIRECTION('center_axis',(0.,1.,0.));
#6213=DIRECTION('ref_axis',(1.,0.,0.));
#7997=CARTESIAN_POINT('',(0.,0.,0.));
#7998=CARTESIAN_POINT('Origin',(0.,32.85,5.52));
#7999=CARTESIAN_POINT('',(0.172988438920056,32.7309411910021,5.52));
#8000=CARTESIAN_POINT('',(0.172988438920056,32.9690588089979,5.52));
#8001=CARTESIAN_POINT('',(0.172988438920056,32.45,5.52));
#8002=CARTESIAN_POINT('Origin',(0.,32.85,5.52));
#8003=CARTESIAN_POINT('Origin',(0.,32.85,5.52));
#8004=CARTESIAN_POINT('',(-0.172988438920056,32.7309411910021,5.52));
#8005=CARTESIAN_POINT('Ctrl Pts',(-0.172988438920059,32.7309411910021,5.52));
#8006=CARTESIAN_POINT('Ctrl Pts',(-0.165594865311318,32.7201985776047,5.52129192197638));
#8007=CARTESIAN_POINT('Ctrl Pts',(-0.157297138725607,32.7103122906273,5.52265394943905));
#8008=CARTESIAN_POINT('Ctrl Pts',(-0.129892073845076,32.6829072257467,5.5267480843909));
#8009=CARTESIAN_POINT('Ctrl Pts',(-0.106330167759285,32.6667579436671,5.52969589327637));
#8010=CARTESIAN_POINT('Ctrl Pts',(-0.0546129046324106,32.6453022060351,
5.53385029472357));
#8011=CARTESIAN_POINT('Ctrl Pts',(-0.0264512308298518,32.64,5.535));
#8012=CARTESIAN_POINT('Ctrl Pts',(0.0264512308298517,32.64,5.535));
#8013=CARTESIAN_POINT('Ctrl Pts',(0.0546129046324105,32.6453022060351,5.53385029472357));
#8014=CARTESIAN_POINT('Ctrl Pts',(0.106330167759285,32.6667579436671,5.52969589327637));
#8015=CARTESIAN_POINT('Ctrl Pts',(0.129892073845076,32.6829072257467,5.5267480843909));
#8016=CARTESIAN_POINT('Ctrl Pts',(0.157297138725608,32.7103122906273,5.52265394943905));
#8017=CARTESIAN_POINT('Ctrl Pts',(0.165594865311314,32.7201985776047,5.52129192197638));
#8018=CARTESIAN_POINT('Ctrl Pts',(0.172988438920054,32.7309411910021,5.52));
#8019=CARTESIAN_POINT('',(-0.21,32.85,5.52));
#8020=CARTESIAN_POINT('Origin',(0.,32.85,5.52));
#8021=CARTESIAN_POINT('',(-0.21,32.85,6.01522725533839));
#8022=CARTESIAN_POINT('',(-0.21,32.85,5.52));
#8023=CARTESIAN_POINT('',(0.21,32.85,6.01522725533839));
#8024=CARTESIAN_POINT('Ctrl Pts',(0.21,32.85,6.01522725533839));
#8025=CARTESIAN_POINT('Ctrl Pts',(0.21,32.8235944730755,6.01522725533839));
#8026=CARTESIAN_POINT('Ctrl Pts',(0.204715737269596,32.7954529259093,6.01600415954412));
#8027=CARTESIAN_POINT('Ctrl Pts',(0.183273763036331,32.7437237310949,6.01880073282317));
#8028=CARTESIAN_POINT('Ctrl Pts',(0.167117923970393,32.720133075872,6.02077897157582));
#8029=CARTESIAN_POINT('Ctrl Pts',(0.129867169887369,32.682882321789,6.02448481141327));
#8030=CARTESIAN_POINT('Ctrl Pts',(0.106276408305765,32.6667262899986,6.02645455657129));
#8031=CARTESIAN_POINT('Ctrl Pts',(0.0545468514058989,32.6452841751738,6.02923165515645));
#8032=CARTESIAN_POINT('Ctrl Pts',(0.0264051785092816,32.64,6.03));
#8033=CARTESIAN_POINT('Ctrl Pts',(-0.0264051785092815,32.64,6.03));
#8034=CARTESIAN_POINT('Ctrl Pts',(-0.0545468514058988,32.6452841751738,
6.02923165515645));
#8035=CARTESIAN_POINT('Ctrl Pts',(-0.106276408305765,32.6667262899986,6.02645455657129));
#8036=CARTESIAN_POINT('Ctrl Pts',(-0.129867169887368,32.682882321789,6.02448481141327));
#8037=CARTESIAN_POINT('Ctrl Pts',(-0.167117923970393,32.720133075872,6.02077897157582));
#8038=CARTESIAN_POINT('Ctrl Pts',(-0.183273763036331,32.7437237310949,6.01880073282317));
#8039=CARTESIAN_POINT('Ctrl Pts',(-0.204715737269596,32.7954529259093,6.01600415954412));
#8040=CARTESIAN_POINT('Ctrl Pts',(-0.210000000000001,32.8235944730755,6.01522725533839));
#8041=CARTESIAN_POINT('Ctrl Pts',(-0.210000000000001,32.85,6.01522725533839));
#8042=CARTESIAN_POINT('Ctrl Pts',(-0.21,32.85,6.01522725533839));
#8043=CARTESIAN_POINT('Ctrl Pts',(-0.21,32.8764055269245,6.01522725533839));
#8044=CARTESIAN_POINT('Ctrl Pts',(-0.204715737269596,32.9045470740907,6.01600415954412));
#8045=CARTESIAN_POINT('Ctrl Pts',(-0.183273763036331,32.9562762689051,6.01880073282317));
#8046=CARTESIAN_POINT('Ctrl Pts',(-0.167117923970393,32.979866924128,6.02077897157582));
#8047=CARTESIAN_POINT('Ctrl Pts',(-0.129867169887369,33.017117678211,6.02448481141327));
#8048=CARTESIAN_POINT('Ctrl Pts',(-0.106276408305765,33.0332737100014,6.02645455657129));
#8049=CARTESIAN_POINT('Ctrl Pts',(-0.0545468514058989,33.0547158248262,
6.02923165515645));
#8050=CARTESIAN_POINT('Ctrl Pts',(-0.0264051785092816,33.06,6.03));
#8051=CARTESIAN_POINT('Ctrl Pts',(0.0264051785092815,33.06,6.03));
#8052=CARTESIAN_POINT('Ctrl Pts',(0.0545468514058988,33.0547158248262,6.02923165515645));
#8053=CARTESIAN_POINT('Ctrl Pts',(0.106276408305765,33.0332737100014,6.02645455657129));
#8054=CARTESIAN_POINT('Ctrl Pts',(0.129867169887368,33.017117678211,6.02448481141327));
#8055=CARTESIAN_POINT('Ctrl Pts',(0.167117923970393,32.979866924128,6.02077897157582));
#8056=CARTESIAN_POINT('Ctrl Pts',(0.183273763036331,32.9562762689051,6.01880073282317));
#8057=CARTESIAN_POINT('Ctrl Pts',(0.204715737269596,32.9045470740907,6.01600415954412));
#8058=CARTESIAN_POINT('Ctrl Pts',(0.21,32.8764055269245,6.01522725533839));
#8059=CARTESIAN_POINT('Ctrl Pts',(0.21,32.85,6.01522725533839));
#8060=CARTESIAN_POINT('',(-0.172988438920056,32.9690588089979,5.52));
#8061=CARTESIAN_POINT('Origin',(0.,32.85,5.52));
#8062=CARTESIAN_POINT('Ctrl Pts',(0.172988438920058,32.9690588089979,5.52));
#8063=CARTESIAN_POINT('Ctrl Pts',(0.165594865311317,32.9798014223953,5.52129192197638));
#8064=CARTESIAN_POINT('Ctrl Pts',(0.157297138725607,32.9896877093727,5.52265394943905));
#8065=CARTESIAN_POINT('Ctrl Pts',(0.129892073845076,33.0170927742533,5.5267480843909));
#8066=CARTESIAN_POINT('Ctrl Pts',(0.106330167759285,33.033242056333,5.52969589327637));
#8067=CARTESIAN_POINT('Ctrl Pts',(0.0546129046324106,33.0546977939649,5.53385029472357));
#8068=CARTESIAN_POINT('Ctrl Pts',(0.0264512308298518,33.06,5.535));
#8069=CARTESIAN_POINT('Ctrl Pts',(-0.0264512308298517,33.06,5.535));
#8070=CARTESIAN_POINT('Ctrl Pts',(-0.0546129046324106,33.0546977939649,
5.53385029472357));
#8071=CARTESIAN_POINT('Ctrl Pts',(-0.106330167759285,33.033242056333,5.52969589327637));
#8072=CARTESIAN_POINT('Ctrl Pts',(-0.129892073845076,33.0170927742533,5.5267480843909));
#8073=CARTESIAN_POINT('Ctrl Pts',(-0.157297138725607,32.9896877093727,5.52265394943905));
#8074=CARTESIAN_POINT('Ctrl Pts',(-0.165594865311317,32.9798014223953,5.52129192197638));
#8075=CARTESIAN_POINT('Ctrl Pts',(-0.172988438920057,32.9690588089979,5.52));
#8076=CARTESIAN_POINT('Origin',(0.,32.85,5.52));
#8077=CARTESIAN_POINT('',(-0.172988438920056,32.45,5.52));
#8078=CARTESIAN_POINT('Origin',(0.,32.45,4.53));
#8079=CARTESIAN_POINT('',(-1.005,33.25,4.53));
#8080=CARTESIAN_POINT('Origin',(0.,33.25,4.53));
#8081=CARTESIAN_POINT('',(-1.005,32.45,4.53));
#8082=CARTESIAN_POINT('',(-1.005,32.45,4.53));
#8083=CARTESIAN_POINT('Origin',(0.,32.45,4.53));
#8084=CARTESIAN_POINT('Origin',(0.,32.45,4.53));
#8085=CARTESIAN_POINT('',(-1.5,33.25,4.53));
#8086=CARTESIAN_POINT('Origin',(0.,33.25,4.53));
#8087=CARTESIAN_POINT('',(-1.5,32.45,4.53));
#8088=CARTESIAN_POINT('',(-1.5,32.45,4.53));
#8089=CARTESIAN_POINT('Origin',(0.,32.45,4.53));
#8090=CARTESIAN_POINT('Origin',(0.,33.25,4.53));
#8091=CARTESIAN_POINT('Origin',(0.,32.45,4.53));
#8339=UNCERTAINTY_MEASURE_WITH_UNIT(LENGTH_MEASURE(0.001),#8378,
'DISTANCE_ACCURACY_VALUE',
'Maximum model space distance between geometric entities at asserted c
onnectivities');
#8345=UNCERTAINTY_MEASURE_WITH_UNIT(LENGTH_MEASURE(0.001),#8378,
'DISTANCE_ACCURACY_VALUE',
'Maximum model space distance between geometric entities at asserted c
onnectivities');
#8371=(
GEOMETRIC_REPRESENTATION_CONTEXT(3)
GLOBAL_UNCERTAINTY_ASSIGNED_CONTEXT((#8339))
GLOBAL_UNIT_ASSIGNED_CONTEXT((#8378,#8380,#8381))
REPRESENTATION_CONTEXT('','3D')
);
#8377=(
GEOMETRIC_REPRESENTATION_CONTEXT(3)
GLOBAL_UNCERTAINTY_ASSIGNED_CONTEXT((#8345))
GLOBAL_UNIT_ASSIGNED_CONTEXT((#8378,#8380,#8381))
REPRESENTATION_CONTEXT('','3D')
);
#8378=(
LENGTH_UNIT()
NAMED_UNIT(*)
SI_UNIT(.CENTI.,.METRE.)
);
#8380=(
NAMED_UNIT(*)
PLANE_ANGLE_UNIT()
SI_UNIT($,.RADIAN.)
);
#8381=(
NAMED_UNIT(*)
SI_UNIT($,.STERADIAN.)
SOLID_ANGLE_UNIT()
);
#8407=SHAPE_DEFINITION_REPRESENTATION(#8474,#8522);
#8474=PRODUCT_DEFINITION_SHAPE('',$,#8554);
#8522=SHAPE_REPRESENTATION('',(#5044),#8371);
#8528=PRODUCT_DEFINITION_CONTEXT('part definition',#8623,'design');
#8554=PRODUCT_DEFINITION('End collar (1)','End collar (1)',#8585,#8528);
#8585=PRODUCT_DEFINITION_FORMATION('',$,#8650);
#8623=APPLICATION_CONTEXT(
'Core Data for Automotive Mechanical Design Process');
#8624=PRODUCT_CONTEXT('part definition',#8623,'mechanical');
#8650=PRODUCT('End collar (1)','End collar (1)','End collar (1)',(#8624));
#8698=COLOUR_RGB('Light Blue',0.38,0.62,0.78);
#8699=FILL_AREA_STYLE_COLOUR('',#8698);
#8700=FILL_AREA_STYLE('',(#8699));
#8701=SURFACE_STYLE_FILL_AREA(#8700);
#8702=SURFACE_SIDE_STYLE('',(#8701));
#8703=SURFACE_STYLE_USAGE(.BOTH.,#8702);
#8704=PRESENTATION_STYLE_ASSIGNMENT((#8703));
ENDSEC;
END-ISO-10303-21;
